ISO-10303-21;
HEADER;
/* Generated by software containing ST-Developer
 * from STEP Tools, Inc. (www.steptools.com) 
 */

FILE_DESCRIPTION(
/* description */ ('Ball-race swivel caster'),
/* implementation_level */ '2;1');

FILE_NAME(
/* name */ 'M4x10 Cap Screw.step',
/* time_stamp */ '2026-10-29T16:15:51-07:00',
/* author */ (''),
/* organization */ (''),
/* preprocessor_version */ 'ST-DEVELOPER v20.2',
/* originating_system */ 'Autodesk Translation Framework v15.17.0.0',
/* authorisation */ '');

FILE_SCHEMA (('AUTOMOTIVE_DESIGN { 1 0 10303 214 3 1 1 }'));
ENDSEC;

DATA;
#10=MECHANICAL_DESIGN_GEOMETRIC_PRESENTATION_REPRESENTATION('',(#319),#7816);
#11=ORIENTED_CLOSED_SHELL('',*,#3725,.F.);
#12=BREP_WITH_VOIDS('Body1',#3726,(#11));
#27=CONICAL_SURFACE('',#4308,0.325,0.785398163397448);
#28=CONICAL_SURFACE('',#4312,0.335,0.785398163397448);
#29=CONICAL_SURFACE('',#4316,0.21,0.463647609000806);
#270=SHAPE_REPRESENTATION_RELATIONSHIP('SRR','None',#7917,#290);
#290=ADVANCED_BREP_SHAPE_REPRESENTATION('',(#12),#7806);
#319=STYLED_ITEM('',(#8104),#12);
#422=FACE_BOUND('',#933,.T.);
#491=PLANE('',#4296);
#492=PLANE('',#4297);
#493=PLANE('',#4298);
#494=PLANE('',#4299);
#495=PLANE('',#4300);
#496=PLANE('',#4301);
#497=PLANE('',#4302);
#498=PLANE('',#4303);
#499=PLANE('',#4304);
#500=PLANE('',#4306);
#501=PLANE('',#4314);
#657=FACE_OUTER_BOUND('',#919,.T.);
#658=FACE_OUTER_BOUND('',#920,.T.);
#659=FACE_OUTER_BOUND('',#921,.T.);
#660=FACE_OUTER_BOUND('',#922,.T.);
#661=FACE_OUTER_BOUND('',#923,.T.);
#662=FACE_OUTER_BOUND('',#924,.T.);
#663=FACE_OUTER_BOUND('',#925,.T.);
#664=FACE_OUTER_BOUND('',#926,.T.);
#665=FACE_OUTER_BOUND('',#927,.T.);
#666=FACE_OUTER_BOUND('',#928,.T.);
#667=FACE_OUTER_BOUND('',#929,.T.);
#668=FACE_OUTER_BOUND('',#930,.T.);
#669=FACE_OUTER_BOUND('',#931,.T.);
#670=FACE_OUTER_BOUND('',#932,.T.);
#671=FACE_OUTER_BOUND('',#934,.T.);
#672=FACE_OUTER_BOUND('',#935,.T.);
#919=EDGE_LOOP('',(#3133,#3134,#3135,#3136));
#920=EDGE_LOOP('',(#3137,#3138,#3139,#3140));
#921=EDGE_LOOP('',(#3141,#3142,#3143,#3144));
#922=EDGE_LOOP('',(#3145,#3146,#3147,#3148));
#923=EDGE_LOOP('',(#3149,#3150,#3151,#3152));
#924=EDGE_LOOP('',(#3153,#3154,#3155,#3156));
#925=EDGE_LOOP('',(#3157,#3158,#3159,#3160,#3161,#3162));
#926=EDGE_LOOP('',(#3163,#3164,#3165,#3166,#3167,#3168));
#927=EDGE_LOOP('',(#3169));
#928=EDGE_LOOP('',(#3170));
#929=EDGE_LOOP('',(#3171,#3172,#3173,#3174));
#930=EDGE_LOOP('',(#3175,#3176,#3177,#3178));
#931=EDGE_LOOP('',(#3179,#3180,#3181,#3182));
#932=EDGE_LOOP('',(#3183));
#933=EDGE_LOOP('',(#3184));
#934=EDGE_LOOP('',(#3185,#3186,#3187,#3188));
#935=EDGE_LOOP('',(#3189,#3190,#3191,#3192));
#1121=LINE('',#7115,#1276);
#1122=LINE('',#7117,#1277);
#1123=LINE('',#7119,#1278);
#1124=LINE('',#7120,#1279);
#1125=LINE('',#7123,#1280);
#1126=LINE('',#7125,#1281);
#1127=LINE('',#7126,#1282);
#1128=LINE('',#7129,#1283);
#1129=LINE('',#7131,#1284);
#1130=LINE('',#7132,#1285);
#1131=LINE('',#7135,#1286);
#1132=LINE('',#7137,#1287);
#1133=LINE('',#7138,#1288);
#1134=LINE('',#7141,#1289);
#1135=LINE('',#7143,#1290);
#1136=LINE('',#7144,#1291);
#1137=LINE('',#7146,#1292);
#1138=LINE('',#7147,#1293);
#1139=LINE('',#7159,#1294);
#1140=LINE('',#7163,#1295);
#1141=LINE('',#7167,#1296);
#1142=LINE('',#7174,#1297);
#1143=LINE('',#7176,#1298);
#1276=VECTOR('',#5269,1.);
#1277=VECTOR('',#5270,1.);
#1278=VECTOR('',#5271,1.);
#1279=VECTOR('',#5272,1.);
#1280=VECTOR('',#5275,1.);
#1281=VECTOR('',#5276,1.);
#1282=VECTOR('',#5277,1.);
#1283=VECTOR('',#5280,1.);
#1284=VECTOR('',#5281,1.);
#1285=VECTOR('',#5282,1.);
#1286=VECTOR('',#5285,1.);
#1287=VECTOR('',#5286,1.);
#1288=VECTOR('',#5287,1.);
#1289=VECTOR('',#5290,1.);
#1290=VECTOR('',#5291,1.);
#1291=VECTOR('',#5292,1.);
#1292=VECTOR('',#5295,1.);
#1293=VECTOR('',#5296,1.);
#1294=VECTOR('',#5313,0.325);
#1295=VECTOR('',#5318,0.35);
#1296=VECTOR('',#5323,0.335);
#1297=VECTOR('',#5332,0.21);
#1298=VECTOR('',#5335,0.2);
#1497=CIRCLE('',#4305,0.1954);
#1498=CIRCLE('',#4307,0.3);
#1499=CIRCLE('',#4309,0.35);
#1500=CIRCLE('',#4311,0.35);
#1501=CIRCLE('',#4313,0.32);
#1502=CIRCLE('',#4315,0.22);
#1503=CIRCLE('',#4317,0.1954);
#1831=VERTEX_POINT('',#7113);
#1832=VERTEX_POINT('',#7114);
#1833=VERTEX_POINT('',#7116);
#1834=VERTEX_POINT('',#7118);
#1835=VERTEX_POINT('',#7122);
#1836=VERTEX_POINT('',#7124);
#1837=VERTEX_POINT('',#7128);
#1838=VERTEX_POINT('',#7130);
#1839=VERTEX_POINT('',#7134);
#1840=VERTEX_POINT('',#7136);
#1841=VERTEX_POINT('',#7140);
#1842=VERTEX_POINT('',#7142);
#1843=VERTEX_POINT('',#7151);
#1844=VERTEX_POINT('',#7154);
#1845=VERTEX_POINT('',#7157);
#1846=VERTEX_POINT('',#7161);
#1847=VERTEX_POINT('',#7165);
#1848=VERTEX_POINT('',#7169);
#1849=VERTEX_POINT('',#7172);
#2286=EDGE_CURVE('',#1831,#1832,#1121,.T.);
#2287=EDGE_CURVE('',#1832,#1833,#1122,.T.);
#2288=EDGE_CURVE('',#1833,#1834,#1123,.T.);
#2289=EDGE_CURVE('',#1831,#1834,#1124,.T.);
#2290=EDGE_CURVE('',#1832,#1835,#1125,.T.);
#2291=EDGE_CURVE('',#1835,#1836,#1126,.T.);
#2292=EDGE_CURVE('',#1836,#1833,#1127,.T.);
#2293=EDGE_CURVE('',#1835,#1837,#1128,.T.);
#2294=EDGE_CURVE('',#1837,#1838,#1129,.T.);
#2295=EDGE_CURVE('',#1838,#1836,#1130,.T.);
#2296=EDGE_CURVE('',#1837,#1839,#1131,.T.);
#2297=EDGE_CURVE('',#1839,#1840,#1132,.T.);
#2298=EDGE_CURVE('',#1840,#1838,#1133,.T.);
#2299=EDGE_CURVE('',#1839,#1841,#1134,.T.);
#2300=EDGE_CURVE('',#1841,#1842,#1135,.T.);
#2301=EDGE_CURVE('',#1842,#1840,#1136,.T.);
#2302=EDGE_CURVE('',#1841,#1831,#1137,.T.);
#2303=EDGE_CURVE('',#1834,#1842,#1138,.T.);
#2304=EDGE_CURVE('',#1843,#1843,#1497,.T.);
#2305=EDGE_CURVE('',#1844,#1844,#1498,.T.);
#2306=EDGE_CURVE('',#1845,#1845,#1499,.T.);
#2307=EDGE_CURVE('',#1845,#1844,#1139,.T.);
#2308=EDGE_CURVE('',#1846,#1846,#1500,.T.);
#2309=EDGE_CURVE('',#1846,#1845,#1140,.T.);
#2310=EDGE_CURVE('',#1847,#1847,#1501,.T.);
#2311=EDGE_CURVE('',#1847,#1846,#1141,.T.);
#2312=EDGE_CURVE('',#1848,#1848,#1502,.T.);
#2313=EDGE_CURVE('',#1849,#1849,#1503,.F.);
#2314=EDGE_CURVE('',#1849,#1848,#1142,.T.);
#2315=EDGE_CURVE('',#1843,#1849,#1143,.T.);
#3133=ORIENTED_EDGE('',*,*,#2286,.T.);
#3134=ORIENTED_EDGE('',*,*,#2287,.T.);
#3135=ORIENTED_EDGE('',*,*,#2288,.T.);
#3136=ORIENTED_EDGE('',*,*,#2289,.F.);
#3137=ORIENTED_EDGE('',*,*,#2290,.T.);
#3138=ORIENTED_EDGE('',*,*,#2291,.T.);
#3139=ORIENTED_EDGE('',*,*,#2292,.T.);
#3140=ORIENTED_EDGE('',*,*,#2287,.F.);
#3141=ORIENTED_EDGE('',*,*,#2293,.T.);
#3142=ORIENTED_EDGE('',*,*,#2294,.T.);
#3143=ORIENTED_EDGE('',*,*,#2295,.T.);
#3144=ORIENTED_EDGE('',*,*,#2291,.F.);
#3145=ORIENTED_EDGE('',*,*,#2296,.T.);
#3146=ORIENTED_EDGE('',*,*,#2297,.T.);
#3147=ORIENTED_EDGE('',*,*,#2298,.T.);
#3148=ORIENTED_EDGE('',*,*,#2294,.F.);
#3149=ORIENTED_EDGE('',*,*,#2299,.T.);
#3150=ORIENTED_EDGE('',*,*,#2300,.T.);
#3151=ORIENTED_EDGE('',*,*,#2301,.T.);
#3152=ORIENTED_EDGE('',*,*,#2297,.F.);
#3153=ORIENTED_EDGE('',*,*,#2302,.T.);
#3154=ORIENTED_EDGE('',*,*,#2289,.T.);
#3155=ORIENTED_EDGE('',*,*,#2303,.T.);
#3156=ORIENTED_EDGE('',*,*,#2300,.F.);
#3157=ORIENTED_EDGE('',*,*,#2302,.F.);
#3158=ORIENTED_EDGE('',*,*,#2299,.F.);
#3159=ORIENTED_EDGE('',*,*,#2296,.F.);
#3160=ORIENTED_EDGE('',*,*,#2293,.F.);
#3161=ORIENTED_EDGE('',*,*,#2290,.F.);
#3162=ORIENTED_EDGE('',*,*,#2286,.F.);
#3163=ORIENTED_EDGE('',*,*,#2303,.F.);
#3164=ORIENTED_EDGE('',*,*,#2288,.F.);
#3165=ORIENTED_EDGE('',*,*,#2292,.F.);
#3166=ORIENTED_EDGE('',*,*,#2295,.F.);
#3167=ORIENTED_EDGE('',*,*,#2298,.F.);
#3168=ORIENTED_EDGE('',*,*,#2301,.F.);
#3169=ORIENTED_EDGE('',*,*,#2304,.F.);
#3170=ORIENTED_EDGE('',*,*,#2305,.F.);
#3171=ORIENTED_EDGE('',*,*,#2306,.F.);
#3172=ORIENTED_EDGE('',*,*,#2307,.T.);
#3173=ORIENTED_EDGE('',*,*,#2305,.T.);
#3174=ORIENTED_EDGE('',*,*,#2307,.F.);
#3175=ORIENTED_EDGE('',*,*,#2308,.F.);
#3176=ORIENTED_EDGE('',*,*,#2309,.T.);
#3177=ORIENTED_EDGE('',*,*,#2306,.T.);
#3178=ORIENTED_EDGE('',*,*,#2309,.F.);
#3179=ORIENTED_EDGE('',*,*,#2310,.F.);
#3180=ORIENTED_EDGE('',*,*,#2311,.T.);
#3181=ORIENTED_EDGE('',*,*,#2308,.T.);
#3182=ORIENTED_EDGE('',*,*,#2311,.F.);
#3183=ORIENTED_EDGE('',*,*,#2310,.T.);
#3184=ORIENTED_EDGE('',*,*,#2312,.F.);
#3185=ORIENTED_EDGE('',*,*,#2313,.F.);
#3186=ORIENTED_EDGE('',*,*,#2314,.T.);
#3187=ORIENTED_EDGE('',*,*,#2312,.T.);
#3188=ORIENTED_EDGE('',*,*,#2314,.F.);
#3189=ORIENTED_EDGE('',*,*,#2304,.T.);
#3190=ORIENTED_EDGE('',*,*,#2315,.T.);
#3191=ORIENTED_EDGE('',*,*,#2313,.T.);
#3192=ORIENTED_EDGE('',*,*,#2315,.F.);
#3475=CYLINDRICAL_SURFACE('',#4310,0.35);
#3476=CYLINDRICAL_SURFACE('',#4318,0.1954);
#3628=ADVANCED_FACE('',(#657),#491,.F.);
#3629=ADVANCED_FACE('',(#658),#492,.F.);
#3630=ADVANCED_FACE('',(#659),#493,.F.);
#3631=ADVANCED_FACE('',(#660),#494,.F.);
#3632=ADVANCED_FACE('',(#661),#495,.F.);
#3633=ADVANCED_FACE('',(#662),#496,.F.);
#3634=ADVANCED_FACE('',(#663),#497,.F.);
#3635=ADVANCED_FACE('',(#664),#498,.F.);
#3636=ADVANCED_FACE('',(#665),#499,.F.);
#3637=ADVANCED_FACE('',(#666),#500,.T.);
#3638=ADVANCED_FACE('',(#667),#27,.T.);
#3639=ADVANCED_FACE('',(#668),#3475,.T.);
#3640=ADVANCED_FACE('',(#669),#28,.T.);
#3641=ADVANCED_FACE('',(#670,#422),#501,.T.);
#3642=ADVANCED_FACE('',(#671),#29,.T.);
#3643=ADVANCED_FACE('',(#672),#3476,.T.);
#3725=CLOSED_SHELL('',(#3628,#3629,#3630,#3631,#3632,#3633,#3634,#3635));
#3726=CLOSED_SHELL('',(#3636,#3637,#3638,#3639,#3640,#3641,#3642,#3643));
#4295=AXIS2_PLACEMENT_3D('',#7111,#5265,#5266);
#4296=AXIS2_PLACEMENT_3D('',#7112,#5267,#5268);
#4297=AXIS2_PLACEMENT_3D('',#7121,#5273,#5274);
#4298=AXIS2_PLACEMENT_3D('',#7127,#5278,#5279);
#4299=AXIS2_PLACEMENT_3D('',#7133,#5283,#5284);
#4300=AXIS2_PLACEMENT_3D('',#7139,#5288,#5289);
#4301=AXIS2_PLACEMENT_3D('',#7145,#5293,#5294);
#4302=AXIS2_PLACEMENT_3D('',#7148,#5297,#5298);
#4303=AXIS2_PLACEMENT_3D('',#7149,#5299,#5300);
#4304=AXIS2_PLACEMENT_3D('',#7150,#5301,#5302);
#4305=AXIS2_PLACEMENT_3D('',#7152,#5303,#5304);
#4306=AXIS2_PLACEMENT_3D('',#7153,#5305,#5306);
#4307=AXIS2_PLACEMENT_3D('',#7155,#5307,#5308);
#4308=AXIS2_PLACEMENT_3D('',#7156,#5309,#5310);
#4309=AXIS2_PLACEMENT_3D('',#7158,#5311,#5312);
#4310=AXIS2_PLACEMENT_3D('',#7160,#5314,#5315);
#4311=AXIS2_PLACEMENT_3D('',#7162,#5316,#5317);
#4312=AXIS2_PLACEMENT_3D('',#7164,#5319,#5320);
#4313=AXIS2_PLACEMENT_3D('',#7166,#5321,#5322);
#4314=AXIS2_PLACEMENT_3D('',#7168,#5324,#5325);
#4315=AXIS2_PLACEMENT_3D('',#7170,#5326,#5327);
#4316=AXIS2_PLACEMENT_3D('',#7171,#5328,#5329);
#4317=AXIS2_PLACEMENT_3D('',#7173,#5330,#5331);
#4318=AXIS2_PLACEMENT_3D('',#7175,#5333,#5334);
#5265=DIRECTION('axis',(0.,0.,1.));
#5266=DIRECTION('refdir',(1.,0.,0.));
#5267=DIRECTION('center_axis',(0.866025403784439,0.,-0.5));
#5268=DIRECTION('ref_axis',(0.5,0.,0.866025403784439));
#5269=DIRECTION('',(-0.5,0.,-0.866025403784439));
#5270=DIRECTION('',(0.,-1.,0.));
#5271=DIRECTION('',(0.5,0.,0.866025403784439));
#5272=DIRECTION('',(0.,-1.,0.));
#5273=DIRECTION('center_axis',(1.60246890531964E-16,0.,-1.));
#5274=DIRECTION('ref_axis',(1.,0.,1.60246890531964E-16));
#5275=DIRECTION('',(-1.,0.,-1.60246890531964E-16));
#5276=DIRECTION('',(0.,-1.,0.));
#5277=DIRECTION('',(1.,0.,1.60246890531964E-16));
#5278=DIRECTION('center_axis',(-0.866025403784439,0.,-0.5));
#5279=DIRECTION('ref_axis',(0.5,0.,-0.866025403784439));
#5280=DIRECTION('',(-0.5,0.,0.866025403784439));
#5281=DIRECTION('',(0.,-1.,0.));
#5282=DIRECTION('',(0.5,0.,-0.866025403784439));
#5283=DIRECTION('center_axis',(-0.866025403784439,0.,0.5));
#5284=DIRECTION('ref_axis',(-0.5,0.,-0.866025403784439));
#5285=DIRECTION('',(0.5,0.,0.866025403784439));
#5286=DIRECTION('',(0.,-1.,0.));
#5287=DIRECTION('',(-0.5,0.,-0.866025403784439));
#5288=DIRECTION('center_axis',(-1.60246890531964E-16,0.,1.));
#5289=DIRECTION('ref_axis',(-1.,0.,-1.60246890531964E-16));
#5290=DIRECTION('',(1.,0.,1.60246890531964E-16));
#5291=DIRECTION('',(0.,-1.,0.));
#5292=DIRECTION('',(-1.,0.,-1.60246890531964E-16));
#5293=DIRECTION('center_axis',(0.866025403784439,0.,0.5));
#5294=DIRECTION('ref_axis',(-0.5,0.,0.866025403784439));
#5295=DIRECTION('',(0.5,0.,-0.866025403784439));
#5296=DIRECTION('',(-0.5,0.,0.866025403784439));
#5297=DIRECTION('center_axis',(0.,1.,0.));
#5298=DIRECTION('ref_axis',(1.,0.,0.));
#5299=DIRECTION('center_axis',(0.,-1.,0.));
#5300=DIRECTION('ref_axis',(0.,0.,-1.));
#5301=DIRECTION('center_axis',(0.,1.,0.));
#5302=DIRECTION('ref_axis',(1.,0.,0.));
#5303=DIRECTION('center_axis',(0.,1.,0.));
#5304=DIRECTION('ref_axis',(1.,0.,0.));
#5305=DIRECTION('center_axis',(0.,1.,0.));
#5306=DIRECTION('ref_axis',(0.,0.,1.));
#5307=DIRECTION('center_axis',(0.,-1.,0.));
#5308=DIRECTION('ref_axis',(1.,0.,0.));
#5309=DIRECTION('center_axis',(0.,-1.,0.));
#5310=DIRECTION('ref_axis',(1.,0.,0.));
#5311=DIRECTION('center_axis',(0.,-1.,0.));
#5312=DIRECTION('ref_axis',(1.,0.,0.));
#5313=DIRECTION('',(0.707106781186547,0.707106781186548,8.65956056235493E-17));
#5314=DIRECTION('center_axis',(0.,-1.,0.));
#5315=DIRECTION('ref_axis',(1.,0.,0.));
#5316=DIRECTION('center_axis',(0.,-1.,0.));
#5317=DIRECTION('ref_axis',(1.,0.,0.));
#5318=DIRECTION('',(0.,1.,0.));
#5319=DIRECTION('center_axis',(0.,1.,0.));
#5320=DIRECTION('ref_axis',(1.,0.,0.));
#5321=DIRECTION('center_axis',(0.,-1.,0.));
#5322=DIRECTION('ref_axis',(1.,0.,0.));
#5323=DIRECTION('',(-0.707106781186547,0.707106781186548,-8.65956056235493E-17));
#5324=DIRECTION('center_axis',(0.,-1.,0.));
#5325=DIRECTION('ref_axis',(0.,0.,-1.));
#5326=DIRECTION('center_axis',(0.,-1.,0.));
#5327=DIRECTION('ref_axis',(1.,0.,0.));
#5328=DIRECTION('center_axis',(0.,1.,0.));
#5329=DIRECTION('ref_axis',(1.,0.,0.));
#5330=DIRECTION('center_axis',(0.,1.,0.));
#5331=DIRECTION('ref_axis',(1.,0.,0.));
#5332=DIRECTION('',(-0.447213595499958,0.894427190999916,-5.47678698264203E-17));
#5333=DIRECTION('center_axis',(0.,-1.,0.));
#5334=DIRECTION('ref_axis',(1.,0.,0.));
#5335=DIRECTION('',(0.,1.,0.));
#7111=CARTESIAN_POINT('',(0.,0.,0.));
#7112=CARTESIAN_POINT('Origin',(0.0866025403784439,-0.4,-0.15));
#7113=CARTESIAN_POINT('',(0.173205080756888,-0.4,0.));
#7114=CARTESIAN_POINT('',(0.0866025403784439,-0.4,-0.15));
#7115=CARTESIAN_POINT('',(0.173205080756888,-0.4,0.));
#7116=CARTESIAN_POINT('',(0.0866025403784439,-0.64,-0.15));
#7117=CARTESIAN_POINT('',(0.0866025403784439,-0.4,-0.15));
#7118=CARTESIAN_POINT('',(0.173205080756888,-0.64,0.));
#7119=CARTESIAN_POINT('',(0.173205080756888,-0.64,0.));
#7120=CARTESIAN_POINT('',(0.173205080756888,-0.4,0.));
#7121=CARTESIAN_POINT('Origin',(-0.0866025403784438,-0.4,-0.15));
#7122=CARTESIAN_POINT('',(-0.0866025403784438,-0.4,-0.15));
#7123=CARTESIAN_POINT('',(0.0866025403784439,-0.4,-0.15));
#7124=CARTESIAN_POINT('',(-0.0866025403784438,-0.64,-0.15));
#7125=CARTESIAN_POINT('',(-0.0866025403784438,-0.4,-0.15));
#7126=CARTESIAN_POINT('',(0.0866025403784439,-0.64,-0.15));
#7127=CARTESIAN_POINT('Origin',(-0.173205080756888,-0.4,-2.77555756156289E-17));
#7128=CARTESIAN_POINT('',(-0.173205080756888,-0.4,-2.12115047744981E-17));
#7129=CARTESIAN_POINT('',(-0.0866025403784438,-0.4,-0.15));
#7130=CARTESIAN_POINT('',(-0.173205080756888,-0.64,-2.77555756156289E-17));
#7131=CARTESIAN_POINT('',(-0.173205080756888,-0.4,-2.12115047744981E-17));
#7132=CARTESIAN_POINT('',(-0.0866025403784438,-0.64,-0.15));
#7133=CARTESIAN_POINT('Origin',(-0.0866025403784439,-0.4,0.15));
#7134=CARTESIAN_POINT('',(-0.0866025403784439,-0.4,0.15));
#7135=CARTESIAN_POINT('',(-0.173205080756888,-0.4,-2.12115047744981E-17));
#7136=CARTESIAN_POINT('',(-0.0866025403784439,-0.64,0.15));
#7137=CARTESIAN_POINT('',(-0.0866025403784439,-0.4,0.15));
#7138=CARTESIAN_POINT('',(-0.173205080756888,-0.64,-2.12115047744981E-17));
#7139=CARTESIAN_POINT('Origin',(0.0866025403784439,-0.4,0.15));
#7140=CARTESIAN_POINT('',(0.0866025403784439,-0.4,0.15));
#7141=CARTESIAN_POINT('',(-0.0866025403784439,-0.4,0.15));
#7142=CARTESIAN_POINT('',(0.0866025403784439,-0.64,0.15));
#7143=CARTESIAN_POINT('',(0.0866025403784439,-0.4,0.15));
#7144=CARTESIAN_POINT('',(-0.0866025403784439,-0.64,0.15));
#7145=CARTESIAN_POINT('Origin',(0.173205080756888,-0.4,0.));
#7146=CARTESIAN_POINT('',(0.0866025403784439,-0.4,0.15));
#7147=CARTESIAN_POINT('',(0.0866025403784439,-0.64,0.15));
#7148=CARTESIAN_POINT('Origin',(0.,-0.4,-2.77555756156289E-17));
#7149=CARTESIAN_POINT('Origin',(0.,-0.64,-2.77555756156289E-17));
#7150=CARTESIAN_POINT('Origin',(0.,-1.,0.));
#7151=CARTESIAN_POINT('',(-0.1954,-1.,2.39295984553393E-17));
#7152=CARTESIAN_POINT('Origin',(0.,-1.,0.));
#7153=CARTESIAN_POINT('Origin',(0.3,0.4,0.));
#7154=CARTESIAN_POINT('',(-0.3,0.4,-3.67394039744206E-17));
#7155=CARTESIAN_POINT('Origin',(0.,0.4,0.));
#7156=CARTESIAN_POINT('Origin',(0.,0.375,0.));
#7157=CARTESIAN_POINT('',(-0.35,0.35,-4.28626379701573E-17));
#7158=CARTESIAN_POINT('Origin',(0.,0.35,0.));
#7159=CARTESIAN_POINT('',(-0.325,0.375,-3.9801020972289E-17));
#7160=CARTESIAN_POINT('Origin',(0.,0.19,0.));
#7161=CARTESIAN_POINT('',(-0.35,0.03,-4.28626379701574E-17));
#7162=CARTESIAN_POINT('Origin',(0.,0.03,0.));
#7163=CARTESIAN_POINT('',(-0.35,0.19,-4.28626379701574E-17));
#7164=CARTESIAN_POINT('Origin',(0.,0.0149999999999999,0.));
#7165=CARTESIAN_POINT('',(-0.32,-3.29597460435593E-17,-3.91886975727153E-17));
#7166=CARTESIAN_POINT('Origin',(0.,0.,0.));
#7167=CARTESIAN_POINT('',(-0.335,0.0149999999999999,-4.10256677714363E-17));
#7168=CARTESIAN_POINT('Origin',(0.22,0.,0.));
#7169=CARTESIAN_POINT('',(-0.22,-6.93889390390723E-18,-2.69422295812418E-17));
#7170=CARTESIAN_POINT('Origin',(0.,0.,0.));
#7171=CARTESIAN_POINT('Origin',(0.,-0.02,0.));
#7172=CARTESIAN_POINT('',(-0.1954,-0.0492,2.39295984553393E-17));
#7173=CARTESIAN_POINT('Origin',(0.,-0.0492,0.));
#7174=CARTESIAN_POINT('',(-0.21,-0.02,-2.57175827820944E-17));
#7175=CARTESIAN_POINT('Origin',(0.,-0.8,0.));
#7176=CARTESIAN_POINT('',(-0.1954,-0.8,-2.39295984553393E-17));
#7779=UNCERTAINTY_MEASURE_WITH_UNIT(LENGTH_MEASURE(0.001),#7817,
'DISTANCE_ACCURACY_VALUE',
'Maximum model space distance between geometric entities at asserted c
onnectivities');
#7789=UNCERTAINTY_MEASURE_WITH_UNIT(LENGTH_MEASURE(0.001),#7817,
'DISTANCE_ACCURACY_VALUE',
'Maximum model space distance between geometric entities at asserted c
onnectivities');
#7806=(
GEOMETRIC_REPRESENTATION_CONTEXT(3)
GLOBAL_UNCERTAINTY_ASSIGNED_CONTEXT((#7779))
GLOBAL_UNIT_ASSIGNED_CONTEXT((#7817,#7819,#7820))
REPRESENTATION_CONTEXT('','3D')
);
#7816=(
GEOMETRIC_REPRESENTATION_CONTEXT(3)
GLOBAL_UNCERTAINTY_ASSIGNED_CONTEXT((#7789))
GLOBAL_UNIT_ASSIGNED_CONTEXT((#7817,#7819,#7820))
REPRESENTATION_CONTEXT('','3D')
);
#7817=(
LENGTH_UNIT()
NAMED_UNIT(*)
SI_UNIT(.CENTI.,.METRE.)
);
#7819=(
NAMED_UNIT(*)
PLANE_ANGLE_UNIT()
SI_UNIT($,.RADIAN.)
);
#7820=(
NAMED_UNIT(*)
SI_UNIT($,.STERADIAN.)
SOLID_ANGLE_UNIT()
);
#7837=SHAPE_DEFINITION_REPRESENTATION(#7871,#7917);
#7871=PRODUCT_DEFINITION_SHAPE('',$,#7944);
#7917=SHAPE_REPRESENTATION('',(#4295),#7806);
#7927=PRODUCT_DEFINITION_CONTEXT('part definition',#8007,'design');
#7944=PRODUCT_DEFINITION('M4x10 Cap Screw','M4x10 Cap Screw',#7970,#7927);
#7970=PRODUCT_DEFINITION_FORMATION('',$,#8025);
#8007=APPLICATION_CONTEXT(
'Core Data for Automotive Mechanical Design Process');
#8008=PRODUCT_CONTEXT('part definition',#8007,'mechanical');
#8025=PRODUCT('M4x10 Cap Screw','M4x10 Cap Screw','M4x10 Cap Screw',(#8008));
#8098=COLOUR_RGB('Black',0.12,0.14,0.17);
#8099=FILL_AREA_STYLE_COLOUR('',#8098);
#8100=FILL_AREA_STYLE('',(#8099));
#8101=SURFACE_STYLE_FILL_AREA(#8100);
#8102=SURFACE_SIDE_STYLE('',(#8101));
#8103=SURFACE_STYLE_USAGE(.BOTH.,#8102);
#8104=PRESENTATION_STYLE_ASSIGNMENT((#8103));
ENDSEC;
END-ISO-10303-21;
